ISO-10303-21;
HEADER;
FILE_DESCRIPTION (('STEP AP214'),
    '1' );
FILE_NAME ('socket.step',
    '2026-10-28T16:30:29',
    ( '' ),
    ( '' ),
    'SwSTEP 2.0',
    'SolidWorks 2025',
    '' );
FILE_SCHEMA (( 'AUTOMOTIVE_DESIGN' ));
ENDSEC;

DATA;
#33=FACE_OUTER_BOUND ( 'NONE', #3649, .T. ) ;
#53=AXIS2_PLACEMENT_3D ( 'NONE', #1297, #6992, #2338 ) ;
#57=DIRECTION ( 'NONE',  ( 1.000000000000000000, 0.000000000000000000, 5.605193857299269528E-45 ) ) ;
#62=DIRECTION ( 'NONE',  ( 0.000000000000000000, 0.000000000000000000, 1.000000000000000000 ) ) ;
#65=FACE_OUTER_BOUND ( 'NONE', #2315, .T. ) ;
#67=TOROIDAL_SURFACE ( 'NONE', #1523, 24.00000000000000000, 3.000000000000000000 ) ;
#76=PRODUCT_DEFINITION_FORMATION_WITH_SPECIFIED_SOURCE ( 'ANY', '', #2239, .NOT_KNOWN. ) ;
#79=VERTEX_POINT ( 'NONE', #3915 ) ;
#91=EDGE_CURVE ( 'NONE', #2680, #1796, #4925, .T. ) ;
#92=FACE_BOUND ( 'NONE', #5400, .T. ) ;
#97=SHAPE_REPRESENTATION ( 'socket', ( #1914 ), #434 ) ;
#102=CARTESIAN_POINT ( 'NONE',  ( -27.00000000000000000, 3.306546357697852550E-15, -3.000000000000002665 ) ) ;
#110=PLANE ( 'NONE',  #3658 ) ;
#114=CARTESIAN_POINT ( 'NONE',  ( -23.99999999999999289, 2.939152317953645922E-15, -3.000000000000002665 ) ) ;
#115=CARTESIAN_POINT ( 'NONE',  ( 0.000000000000000000, 0.000000000000000000, 0.000000000000000000 ) ) ;
#118=ORIENTED_EDGE ( 'NONE', *, *, #6512, .T. ) ;
#141=FACE_OUTER_BOUND ( 'NONE', #3804, .T. ) ;
#177=STYLED_ITEM('',(#7652),#6264);
#190=ORIENTED_EDGE ( 'NONE', *, *, #5818, .T. ) ;
#213=CARTESIAN_POINT ( 'NONE',  ( 0.000000000000000000, 0.000000000000000000, -3.000000000000002665 ) ) ;
#222=DIRECTION ( 'NONE',  ( 1.000000000000000000, 0.000000000000000000, 0.000000000000000000 ) ) ;
#226=DIRECTION ( 'NONE',  ( 1.000000000000000000, 0.000000000000000000, 0.000000000000000000 ) ) ;
#227=ORIENTED_EDGE ( 'NONE', *, *, #91, .T. ) ;
#268=ORIENTED_EDGE ( 'NONE', *, *, #1167, .T. ) ;
#289=CARTESIAN_POINT ( 'NONE',  ( 13.99999999999999645, 0.000000000000000000, -39.99999999999997868 ) ) ;
#296=CIRCLE ( 'NONE', #4727, 23.99999999999999289 ) ;
#316=VERTEX_POINT ( 'NONE', #2557 ) ;
#320=DIRECTION ( 'NONE',  ( 5.605193857299270773E-45, 0.000000000000000000, 1.000000000000000000 ) ) ;
#344=ORIENTED_EDGE ( 'NONE', *, *, #6723, .F. ) ;
#345=ADVANCED_FACE ( 'NONE', ( #141 ), #4259, .T. ) ;
#369=AXIS2_PLACEMENT_3D ( 'NONE', #2064, #7334, #2026 ) ;
#434=( GEOMETRIC_REPRESENTATION_CONTEXT ( 3 ) GLOBAL_UNCERTAINTY_ASSIGNED_CONTEXT ( ( #6415 ) ) GLOBAL_UNIT_ASSIGNED_CONTEXT ( ( #1708, #3828, #5557 ) ) REPRESENTATION_CONTEXT ( 'NONE', 'WORKASPACE' ) );
#491=ORIENTED_EDGE ( 'NONE', *, *, #3019, .T. ) ;
#555=FACE_OUTER_BOUND ( 'NONE', #4424, .T. ) ;
#596=ADVANCED_BREP_SHAPE_REPRESENTATION ( '', ( #6264, #1914 ), #434 ) ;
#619=ORIENTED_EDGE ( 'NONE', *, *, #2332, .F. ) ;
#622=EDGE_LOOP ( 'NONE', ( #2754, #118 ) ) ;
#665=AXIS2_PLACEMENT_3D ( 'NONE', #5893, #7160, #3594 ) ;
#670=DIRECTION ( 'NONE',  ( 1.000000000000000000, 0.000000000000000000, 0.000000000000000000 ) ) ;
#685=ORIENTED_EDGE ( 'NONE', *, *, #2916, .F. ) ;
#693=AXIS2_PLACEMENT_3D ( 'NONE', #2604, #2683, #5730 ) ;
#741=PLANE ( 'NONE',  #7336 ) ;
#769=ORIENTED_EDGE ( 'NONE', *, *, #1167, .F. ) ;
#790=DIRECTION ( 'NONE',  ( 5.605193857299270773E-45, 0.000000000000000000, 1.000000000000000000 ) ) ;
#815=ADVANCED_FACE ( 'NONE', ( #6736 ), #3707, .T. ) ;
#823=CARTESIAN_POINT ( 'NONE',  ( 0.000000000000000000, 0.000000000000000000, 0.000000000000000000 ) ) ;
#872=CARTESIAN_POINT ( 'NONE',  ( 23.99999999999999289, 0.000000000000000000, -9.999999999999994671 ) ) ;
#921=EDGE_CURVE ( 'NONE', #1151, #2680, #4398, .T. ) ;
#930=FACE_OUTER_BOUND ( 'NONE', #2463, .T. ) ;
#994=ORIENTED_EDGE ( 'NONE', *, *, #1081, .T. ) ;
#1011=ORIENTED_EDGE ( 'NONE', *, *, #5498, .T. ) ;
#1081=EDGE_CURVE ( 'NONE', #6577, #5363, #1856, .T. ) ;
#1150=CARTESIAN_POINT ( 'NONE',  ( 0.000000000000000000, 0.000000000000000000, -9.999999999999994671 ) ) ;
#1151=VERTEX_POINT ( 'NONE', #7194 ) ;
#1167=EDGE_CURVE ( 'NONE', #1151, #316, #1860, .T. ) ;
#1224=LINE ( 'NONE', #3583, #5091 ) ;
#1227=CIRCLE ( 'NONE', #5532, 23.99999999999999289 ) ;
#1237=SHAPE_DEFINITION_REPRESENTATION ( #6357, #97 ) ;
#1269=VERTEX_POINT ( 'NONE', #1359 ) ;
#1270=APPLICATION_CONTEXT ( 'automotive_design' ) ;
#1271=ADVANCED_FACE ( 'NONE', ( #2483 ), #110, .F. ) ;
#1279=( GEOMETRIC_REPRESENTATION_CONTEXT ( 3 ) GLOBAL_UNCERTAINTY_ASSIGNED_CONTEXT ( ( #5800 ) ) GLOBAL_UNIT_ASSIGNED_CONTEXT ( ( #6568, #4693, #4223 ) ) REPRESENTATION_CONTEXT ( 'NONE', 'WORKASPACE' ) );
#1297=CARTESIAN_POINT ( 'NONE',  ( 23.99999999999999289, 0.000000000000000000, -3.000000000000002665 ) ) ;
#1306=EDGE_CURVE ( 'NONE', #2624, #4861, #6843, .T. ) ;
#1321=CYLINDRICAL_SURFACE ( 'NONE', #2019, 26.99999999999999289 ) ;
#1359=CARTESIAN_POINT ( 'NONE',  ( -14.00000000000000000, 1.714505518806294046E-15, -39.99999999999997868 ) ) ;
#1390=AXIS2_PLACEMENT_3D ( 'NONE', #4789, #5398, #7123 ) ;
#1414=PRODUCT_DEFINITION ( 'UNKNOWN', '', #76, #2409 ) ;
#1439=ORIENTED_EDGE ( 'NONE', *, *, #6492, .T. ) ;
#1461=ORIENTED_EDGE ( 'NONE', *, *, #6852, .T. ) ;
#1482=AXIS2_PLACEMENT_3D ( 'NONE', #1769, #4126, #3003 ) ;
#1523=AXIS2_PLACEMENT_3D ( 'NONE', #7057, #2327, #1789 ) ;
#1525=DIRECTION ( 'NONE',  ( 0.000000000000000000, -1.000000000000000000, 0.000000000000000000 ) ) ;
#1526=ORIENTED_EDGE ( 'NONE', *, *, #1961, .F. ) ;
#1529=VERTEX_POINT ( 'NONE', #289 ) ;
#1551=CARTESIAN_POINT ( 'NONE',  ( 13.99999999999999645, 0.000000000000000000, -9.999999999999994671 ) ) ;
#1610=LINE ( 'NONE', #6314, #5723 ) ;
#1611=ORIENTED_EDGE ( 'NONE', *, *, #5498, .F. ) ;
#1708=( LENGTH_UNIT ( ) NAMED_UNIT ( * ) SI_UNIT ( .MILLI., .METRE. ) );
#1749=CARTESIAN_POINT ( 'NONE',  ( 0.000000000000000000, 0.000000000000000000, 0.000000000000000000 ) ) ;
#1756=DIRECTION ( 'NONE',  ( 1.000000000000000000, 0.000000000000000000, -5.605193857299270773E-45 ) ) ;
#1763=ADVANCED_FACE ( 'NONE', ( #5324, #2516 ), #741, .F. ) ;
#1769=CARTESIAN_POINT ( 'NONE',  ( 0.000000000000000000, 0.000000000000000000, -6.999999999999992006 ) ) ;
#1780=AXIS2_PLACEMENT_3D ( 'NONE', #7555, #5903, #6983 ) ;
#1789=DIRECTION ( 'NONE',  ( 1.000000000000000000, 0.000000000000000000, -5.605193857299270773E-45 ) ) ;
#1796=VERTEX_POINT ( 'NONE', #102 ) ;
#1818=CYLINDRICAL_SURFACE ( 'NONE', #665, 17.99999999999999645 ) ;
#1848=ORIENTED_EDGE ( 'NONE', *, *, #5539, .T. ) ;
#1856=CIRCLE ( 'NONE', #3591, 17.99999999999999645 ) ;
#1860=CIRCLE ( 'NONE', #1482, 26.99999999999999289 ) ;
#1864=DIRECTION ( 'NONE',  ( 1.000000000000000000, 0.000000000000000000, 0.000000000000000000 ) ) ;
#1904=DIRECTION ( 'NONE',  ( 1.000000000000000000, 0.000000000000000000, 5.605193857299269528E-45 ) ) ;
#1914=AXIS2_PLACEMENT_3D ( 'NONE', #1749, #62, #1864 ) ;
#1923=CIRCLE ( 'NONE', #693, 26.99999999999999289 ) ;
#1943=ORIENTED_EDGE ( 'NONE', *, *, #6546, .T. ) ;
#1961=EDGE_CURVE ( 'NONE', #79, #7476, #2664, .T. ) ;
#1972=CARTESIAN_POINT ( 'NONE',  ( 0.000000000000000000, 0.000000000000000000, -9.999999999999994671 ) ) ;
#2019=AXIS2_PLACEMENT_3D ( 'NONE', #1972, #6560, #5406 ) ;
#2020=ADVANCED_FACE ( 'NONE', ( #33 ), #5272, .T. ) ;
#2026=DIRECTION ( 'NONE',  ( 1.000000000000000000, 0.000000000000000000, 0.000000000000000000 ) ) ;
#2028=AXIS2_PLACEMENT_3D ( 'NONE', #4346, #3847, #7375 ) ;
#2039=ORIENTED_EDGE ( 'NONE', *, *, #6512, .F. ) ;
#2064=CARTESIAN_POINT ( 'NONE',  ( 0.000000000000000000, 0.000000000000000000, -3.000000000000002665 ) ) ;
#2094=ORIENTED_EDGE ( 'NONE', *, *, #5015, .T. ) ;
#2132=LINE ( 'NONE', #5674, #4242 ) ;
#2151=CARTESIAN_POINT ( 'NONE',  ( -24.00000000000000000, 3.122849337825749433E-15, -1.540743955509789033E-30 ) ) ;
#2239=PRODUCT ( 'socket', 'socket', '', ( #5283 ) ) ;
#2273=ORIENTED_EDGE ( 'NONE', *, *, #2332, .T. ) ;
#2278=CARTESIAN_POINT ( 'NONE',  ( 17.99999999999999645, 0.000000000000000000, -39.99999999999997868 ) ) ;
#2315=EDGE_LOOP ( 'NONE', ( #190, #1461 ) ) ;
#2327=DIRECTION ( 'NONE',  ( 5.605193857299270773E-45, 0.000000000000000000, 1.000000000000000000 ) ) ;
#2332=EDGE_CURVE ( 'NONE', #316, #1151, #1923, .T. ) ;
#2337=CARTESIAN_POINT ( 'NONE',  ( 0.000000000000000000, 0.000000000000000000, -6.999999999999992006 ) ) ;
#2338=DIRECTION ( 'NONE',  ( 0.000000000000000000, 0.000000000000000000, -1.000000000000000000 ) ) ;
#2407=PLANE ( 'NONE',  #6261 ) ;
#2409=PRODUCT_DEFINITION_CONTEXT ( 'detailed design', #7413, 'design' ) ;
#2432=PLANE ( 'NONE',  #1390 ) ;
#2463=EDGE_LOOP ( 'NONE', ( #344, #4044, #6465, #3676 ) ) ;
#2467=EDGE_LOOP ( 'NONE', ( #6362, #1439, #769, #685 ) ) ;
#2483=FACE_OUTER_BOUND ( 'NONE', #6804, .T. ) ;
#2512=AXIS2_PLACEMENT_3D ( 'NONE', #6237, #5704, #4553 ) ;
#2516=FACE_OUTER_BOUND ( 'NONE', #3903, .T. ) ;
#2545=ADVANCED_FACE ( 'NONE', ( #4263 ), #2988, .F. ) ;
#2554=DIRECTION ( 'NONE',  ( -5.605193857299270773E-45, -0.000000000000000000, -1.000000000000000000 ) ) ;
#2557=CARTESIAN_POINT ( 'NONE',  ( -27.00000000000000000, 3.306546357697852550E-15, -6.999999999999992006 ) ) ;
#2571=EDGE_CURVE ( 'NONE', #5363, #6577, #5306, .T. ) ;
#2582=AXIS2_PLACEMENT_3D ( 'NONE', #5030, #3728, #226 ) ;
#2604=CARTESIAN_POINT ( 'NONE',  ( 0.000000000000000000, 0.000000000000000000, -6.999999999999992006 ) ) ;
#2607=CARTESIAN_POINT ( 'NONE',  ( 23.99999999999999289, 0.000000000000000000, -6.999999999999992006 ) ) ;
#2624=VERTEX_POINT ( 'NONE', #6750 ) ;
#2648=DIRECTION ( 'NONE',  ( 5.605193857299270773E-45, 0.000000000000000000, 1.000000000000000000 ) ) ;
#2649=DIRECTION ( 'NONE',  ( 0.000000000000000000, 0.000000000000000000, -1.000000000000000000 ) ) ;
#2660=DIRECTION ( 'NONE',  ( 1.000000000000000000, 0.000000000000000000, 0.000000000000000000 ) ) ;
#2664=CIRCLE ( 'NONE', #4159, 13.99999999999999645 ) ;
#2680=VERTEX_POINT ( 'NONE', #4835 ) ;
#2683=DIRECTION ( 'NONE',  ( 5.605193857299270773E-45, 0.000000000000000000, 1.000000000000000000 ) ) ;
#2685=LINE ( 'NONE', #3772, #6662 ) ;
#2691=CARTESIAN_POINT ( 'NONE',  ( 0.000000000000000000, 0.000000000000000000, -3.000000000000002665 ) ) ;
#2697=CARTESIAN_POINT ( 'NONE',  ( 0.000000000000000000, 0.000000000000000000, -3.000000000000002665 ) ) ;
#2754=ORIENTED_EDGE ( 'NONE', *, *, #3348, .T. ) ;
#2796=VERTEX_POINT ( 'NONE', #6858 ) ;
#2847=EDGE_LOOP ( 'NONE', ( #2094, #6995 ) ) ;
#2850=EDGE_LOOP ( 'NONE', ( #2039, #1011, #6901, #3844 ) ) ;
#2858=VERTEX_POINT ( 'NONE', #6162 ) ;
#2859=ORIENTED_EDGE ( 'NONE', *, *, #1306, .F. ) ;
#2882=AXIS2_PLACEMENT_3D ( 'NONE', #3452, #5870, #2979 ) ;
#2912=DIRECTION ( 'NONE',  ( -1.000000000000000000, 1.224646799147353454E-16, 0.000000000000000000 ) ) ;
#2916=EDGE_CURVE ( 'NONE', #5534, #1151, #2975, .T. ) ;
#2975=CIRCLE ( 'NONE', #5558, 2.999999999999999112 ) ;
#2979=DIRECTION ( 'NONE',  ( 1.000000000000000000, 0.000000000000000000, 0.000000000000000000 ) ) ;
#2988=CYLINDRICAL_SURFACE ( 'NONE', #5672, 13.99999999999999645 ) ;
#2997=DIRECTION ( 'NONE',  ( 5.605193857299270773E-45, 0.000000000000000000, 1.000000000000000000 ) ) ;
#2999=DIRECTION ( 'NONE',  ( 5.605193857299270773E-45, 0.000000000000000000, 1.000000000000000000 ) ) ;
#3003=DIRECTION ( 'NONE',  ( 1.000000000000000000, 0.000000000000000000, 0.000000000000000000 ) ) ;
#3019=EDGE_CURVE ( 'NONE', #5363, #4861, #2685, .T. ) ;
#3035=DIRECTION ( 'NONE',  ( 1.000000000000000000, 0.000000000000000000, 5.605193857299269528E-45 ) ) ;
#3060=DIRECTION ( 'NONE',  ( -5.605193857299269528E-45, 0.000000000000000000, 1.000000000000000000 ) ) ;
#3063=ORIENTED_EDGE ( 'NONE', *, *, #921, .F. ) ;
#3174=VERTEX_POINT ( 'NONE', #2151 ) ;
#3256=CIRCLE ( 'NONE', #5095, 26.99999999999999289 ) ;
#3268=CARTESIAN_POINT ( 'NONE',  ( 13.99999999999999645, 0.000000000000000000, -39.99999999999997868 ) ) ;
#3348=EDGE_CURVE ( 'NONE', #1529, #1269, #4926, .T. ) ;
#3399=DIRECTION ( 'NONE',  ( 1.000000000000000000, 0.000000000000000000, 0.000000000000000000 ) ) ;
#3406=ORIENTED_EDGE ( 'NONE', *, *, #6395, .T. ) ;
#3452=CARTESIAN_POINT ( 'NONE',  ( 0.000000000000000000, 0.000000000000000000, -9.999999999999994671 ) ) ;
#3475=CARTESIAN_POINT ( 'NONE',  ( 17.99999999999999645, 0.000000000000000000, -9.999999999999994671 ) ) ;
#3484=DIRECTION ( 'NONE',  ( 5.605193857299270773E-45, 0.000000000000000000, 1.000000000000000000 ) ) ;
#3512=CIRCLE ( 'NONE', #7414, 13.99999999999999645 ) ;
#3513=AXIS2_PLACEMENT_3D ( 'NONE', #2337, #7030, #1756 ) ;
#3519=ORIENTED_EDGE ( 'NONE', *, *, #3019, .F. ) ;
#3538=DIRECTION ( 'NONE',  ( 5.605193857299270773E-45, 0.000000000000000000, 1.000000000000000000 ) ) ;
#3583=CARTESIAN_POINT ( 'NONE',  ( -13.99999999999999645, 1.714505518806293652E-15, -39.99999999999997868 ) ) ;
#3591=AXIS2_PLACEMENT_3D ( 'NONE', #5741, #6270, #5855 ) ;
#3594=DIRECTION ( 'NONE',  ( 1.000000000000000000, 0.000000000000000000, 0.000000000000000000 ) ) ;
#3605=CARTESIAN_POINT ( 'NONE',  ( 0.000000000000000000, 0.000000000000000000, -39.99999999999997868 ) ) ;
#3631=TOROIDAL_SURFACE ( 'NONE', #4243, 24.00000000000000000, 3.000000000000000000 ) ;
#3649=EDGE_LOOP ( 'NONE', ( #268, #3406, #6234, #3063 ) ) ;
#3653=DIRECTION ( 'NONE',  ( 1.000000000000000000, 0.000000000000000000, 0.000000000000000000 ) ) ;
#3654=DIRECTION ( 'NONE',  ( 1.224646799147352714E-16, 1.000000000000000000, -6.864382715941954980E-61 ) ) ;
#3658=AXIS2_PLACEMENT_3D ( 'NONE', #4771, #4839, #5452 ) ;
#3660=EDGE_LOOP ( 'NONE', ( #3805, #994, #491, #2859 ) ) ;
#3676=ORIENTED_EDGE ( 'NONE', *, *, #5864, .F. ) ;
#3707=TOROIDAL_SURFACE ( 'NONE', #6407, 24.00000000000000000, 3.000000000000000000 ) ;
#3721=ADVANCED_FACE ( 'NONE', ( #65 ), #2407, .T. ) ;
#3728=DIRECTION ( 'NONE',  ( 5.605193857299270773E-45, 0.000000000000000000, 1.000000000000000000 ) ) ;
#3767=EDGE_CURVE ( 'NONE', #2796, #5534, #1227, .T. ) ;
#3772=CARTESIAN_POINT ( 'NONE',  ( 17.99999999999999645, 0.000000000000000000, -39.99999999999997868 ) ) ;
#3804=EDGE_LOOP ( 'NONE', ( #6837, #5275, #7234, #3519 ) ) ;
#3805=ORIENTED_EDGE ( 'NONE', *, *, #4421, .F. ) ;
#3812=CLOSED_SHELL ( 'NONE', ( #7317, #6887, #2545, #345, #2020, #6609, #5031, #3721, #4981, #1763, #5581, #1271, #815, #6545 ) ) ;
#3823=CARTESIAN_POINT ( 'NONE',  ( 0.000000000000000000, 0.000000000000000000, -9.999999999999994671 ) ) ;
#3828=( NAMED_UNIT ( * ) PLANE_ANGLE_UNIT ( ) SI_UNIT ( $, .RADIAN. ) );
#3831=DIRECTION ( 'NONE',  ( 1.000000000000000000, 0.000000000000000000, 0.000000000000000000 ) ) ;
#3844=ORIENTED_EDGE ( 'NONE', *, *, #5539, .F. ) ;
#3847=DIRECTION ( 'NONE',  ( 5.605193857299270773E-45, 0.000000000000000000, 1.000000000000000000 ) ) ;
#3871=CIRCLE ( 'NONE', #1780, 2.999999999999999112 ) ;
#3903=EDGE_LOOP ( 'NONE', ( #6108, #6109 ) ) ;
#3915=CARTESIAN_POINT ( 'NONE',  ( -14.00000000000000000, 1.714505518806294046E-15, -9.999999999999994671 ) ) ;
#4002=CIRCLE ( 'NONE', #4486, 2.999999999999999112 ) ;
#4013=DIRECTION ( 'NONE',  ( 5.605193857299270773E-45, 0.000000000000000000, 1.000000000000000000 ) ) ;
#4020=ORIENTED_EDGE ( 'NONE', *, *, #6492, .F. ) ;
#4044=ORIENTED_EDGE ( 'NONE', *, *, #7295, .T. ) ;
#4099=FACE_OUTER_BOUND ( 'NONE', #6647, .T. ) ;
#4126=DIRECTION ( 'NONE',  ( 5.605193857299270773E-45, 0.000000000000000000, 1.000000000000000000 ) ) ;
#4141=CARTESIAN_POINT ( 'NONE',  ( -18.00000000000000000, 2.204364238465234639E-15, -39.99999999999997868 ) ) ;
#4148=AXIS2_PLACEMENT_3D ( 'NONE', #4190, #7177, #6494 ) ;
#4159=AXIS2_PLACEMENT_3D ( 'NONE', #3823, #6157, #2660 ) ;
#4190=CARTESIAN_POINT ( 'NONE',  ( 0.000000000000000000, 0.000000000000000000, -9.999999999999994671 ) ) ;
#4223=( NAMED_UNIT ( * ) SI_UNIT ( $, .STERADIAN. ) SOLID_ANGLE_UNIT ( ) );
#4242=VECTOR ( 'NONE', #6865, 1000.000000000000000 ) ;
#4243=AXIS2_PLACEMENT_3D ( 'NONE', #2697, #320, #7388 ) ;
#4246=DIRECTION ( 'NONE',  ( 1.000000000000000000, 0.000000000000000000, 0.000000000000000000 ) ) ;
#4259=CYLINDRICAL_SURFACE ( 'NONE', #7013, 17.99999999999999645 ) ;
#4263=FACE_OUTER_BOUND ( 'NONE', #2850, .T. ) ;
#4346=CARTESIAN_POINT ( 'NONE',  ( 0.000000000000000000, 0.000000000000000000, -39.99999999999997868 ) ) ;
#4368=CIRCLE ( 'NONE', #2882, 17.99999999999999645 ) ;
#4372=ORIENTED_EDGE ( 'NONE', *, *, #4471, .T. ) ;
#4398=LINE ( 'NONE', #5658, #5663 ) ;
#4421=EDGE_CURVE ( 'NONE', #6577, #2624, #1610, .T. ) ;
#4424=EDGE_LOOP ( 'NONE', ( #4020, #4438, #5775, #619 ) ) ;
#4438=ORIENTED_EDGE ( 'NONE', *, *, #5015, .F. ) ;
#4471=EDGE_CURVE ( 'NONE', #7476, #79, #3512, .T. ) ;
#4478=MECHANICAL_DESIGN_GEOMETRIC_PRESENTATION_REPRESENTATION('',(#177),#1279);
#4486=AXIS2_PLACEMENT_3D ( 'NONE', #114, #3654, #2912 ) ;
#4553=DIRECTION ( 'NONE',  ( 1.000000000000000000, 0.000000000000000000, 5.605193857299269528E-45 ) ) ;
#4598=CIRCLE ( 'NONE', #6683, 23.99999999999999289 ) ;
#4693=( NAMED_UNIT ( * ) PLANE_ANGLE_UNIT ( ) SI_UNIT ( $, .RADIAN. ) );
#4727=AXIS2_PLACEMENT_3D ( 'NONE', #6008, #5316, #4246 ) ;
#4743=AXIS2_PLACEMENT_3D ( 'NONE', #5254, #3484, #670 ) ;
#4771=CARTESIAN_POINT ( 'NONE',  ( 0.000000000000000000, 0.000000000000000000, -9.999999999999994671 ) ) ;
#4789=CARTESIAN_POINT ( 'NONE',  ( 0.000000000000000000, 0.000000000000000000, -9.999999999999994671 ) ) ;
#4805=FACE_OUTER_BOUND ( 'NONE', #2467, .T. ) ;
#4835=CARTESIAN_POINT ( 'NONE',  ( 26.99999999999999289, 0.000000000000000000, -3.000000000000002665 ) ) ;
#4839=DIRECTION ( 'NONE',  ( -5.605193857299269528E-45, 0.000000000000000000, 1.000000000000000000 ) ) ;
#4860=CIRCLE ( 'NONE', #2512, 23.99999999999999289 ) ;
#4861=VERTEX_POINT ( 'NONE', #3475 ) ;
#4863=FACE_OUTER_BOUND ( 'NONE', #3660, .T. ) ;
#4869=TOROIDAL_SURFACE ( 'NONE', #3513, 24.00000000000000000, 3.000000000000000000 ) ;
#4873=DIRECTION ( 'NONE',  ( 1.000000000000000000, 0.000000000000000000, 0.000000000000000000 ) ) ;
#4890=LINE ( 'NONE', #3268, #7055 ) ;
#4925=CIRCLE ( 'NONE', #369, 26.99999999999999289 ) ;
#4926=CIRCLE ( 'NONE', #2582, 13.99999999999999645 ) ;
#4975=DIRECTION ( 'NONE',  ( 1.000000000000000000, 0.000000000000000000, -5.605193857299270773E-45 ) ) ;
#4981=ADVANCED_FACE ( 'NONE', ( #4863 ), #1818, .T. ) ;
#5015=EDGE_CURVE ( 'NONE', #5534, #2796, #296, .T. ) ;
#5030=CARTESIAN_POINT ( 'NONE',  ( 0.000000000000000000, 0.000000000000000000, -39.99999999999997868 ) ) ;
#5031=ADVANCED_FACE ( 'NONE', ( #5361, #92 ), #2432, .F. ) ;
#5036=FACE_OUTER_BOUND ( 'NONE', #5279, .T. ) ;
#5091=VECTOR ( 'NONE', #2999, 1000.000000000000000 ) ;
#5095=AXIS2_PLACEMENT_3D ( 'NONE', #213, #2554, #4873 ) ;
#5254=CARTESIAN_POINT ( 'NONE',  ( 0.000000000000000000, 0.000000000000000000, -39.99999999999997868 ) ) ;
#5272=CYLINDRICAL_SURFACE ( 'NONE', #6361, 26.99999999999999289 ) ;
#5275=ORIENTED_EDGE ( 'NONE', *, *, #4421, .T. ) ;
#5279=EDGE_LOOP ( 'NONE', ( #1611, #6230, #1848, #4372 ) ) ;
#5283=PRODUCT_CONTEXT ( 'NONE', #1270, 'mechanical' ) ;
#5305=CARTESIAN_POINT ( 'NONE',  ( 0.000000000000000000, 0.000000000000000000, -9.999999999999994671 ) ) ;
#5306=CIRCLE ( 'NONE', #6656, 17.99999999999999645 ) ;
#5316=DIRECTION ( 'NONE',  ( -5.605193857299270773E-45, -0.000000000000000000, -1.000000000000000000 ) ) ;
#5324=FACE_BOUND ( 'NONE', #622, .T. ) ;
#5361=FACE_OUTER_BOUND ( 'NONE', #2847, .T. ) ;
#5363=VERTEX_POINT ( 'NONE', #2278 ) ;
#5370=CARTESIAN_POINT ( 'NONE',  ( 0.000000000000000000, 0.000000000000000000, -39.99999999999997868 ) ) ;
#5380=DIRECTION ( 'NONE',  ( 5.605193857299270773E-45, 0.000000000000000000, 1.000000000000000000 ) ) ;
#5396=ORIENTED_EDGE ( 'NONE', *, *, #5864, .T. ) ;
#5398=DIRECTION ( 'NONE',  ( -5.605193857299269528E-45, 0.000000000000000000, 1.000000000000000000 ) ) ;
#5400=EDGE_LOOP ( 'NONE', ( #1943, #7122 ) ) ;
#5406=DIRECTION ( 'NONE',  ( 1.000000000000000000, 0.000000000000000000, 0.000000000000000000 ) ) ;
#5450=CARTESIAN_POINT ( 'NONE',  ( 0.000000000000000000, 0.000000000000000000, -9.999999999999994671 ) ) ;
#5452=DIRECTION ( 'NONE',  ( 1.000000000000000000, 0.000000000000000000, 5.605193857299269528E-45 ) ) ;
#5477=ORIENTED_EDGE ( 'NONE', *, *, #4471, .F. ) ;
#5498=EDGE_CURVE ( 'NONE', #1269, #79, #1224, .T. ) ;
#5532=AXIS2_PLACEMENT_3D ( 'NONE', #5450, #5561, #3831 ) ;
#5534=VERTEX_POINT ( 'NONE', #872 ) ;
#5539=EDGE_CURVE ( 'NONE', #1529, #7476, #4890, .T. ) ;
#5557=( NAMED_UNIT ( * ) SI_UNIT ( $, .STERADIAN. ) SOLID_ANGLE_UNIT ( ) );
#5558=AXIS2_PLACEMENT_3D ( 'NONE', #2607, #1525, #2649 ) ;
#5561=DIRECTION ( 'NONE',  ( -5.605193857299270773E-45, -0.000000000000000000, -1.000000000000000000 ) ) ;
#5575=CYLINDRICAL_SURFACE ( 'NONE', #2028, 13.99999999999999645 ) ;
#5581=ADVANCED_FACE ( 'NONE', ( #5036 ), #5575, .F. ) ;
#5658=CARTESIAN_POINT ( 'NONE',  ( 26.99999999999999289, 0.000000000000000000, -9.999999999999994671 ) ) ;
#5663=VECTOR ( 'NONE', #6151, 1000.000000000000000 ) ;
#5672=AXIS2_PLACEMENT_3D ( 'NONE', #7178, #5380, #3653 ) ;
#5674=CARTESIAN_POINT ( 'NONE',  ( -26.99999999999999289, 3.306546357697851761E-15, -9.999999999999994671 ) ) ;
#5704=DIRECTION ( 'NONE',  ( 5.605193857299270773E-45, 0.000000000000000000, 1.000000000000000000 ) ) ;
#5723=VECTOR ( 'NONE', #4013, 1000.000000000000000 ) ;
#5730=DIRECTION ( 'NONE',  ( 1.000000000000000000, 0.000000000000000000, 0.000000000000000000 ) ) ;
#5741=CARTESIAN_POINT ( 'NONE',  ( 0.000000000000000000, 0.000000000000000000, -39.99999999999997868 ) ) ;
#5775=ORIENTED_EDGE ( 'NONE', *, *, #2916, .T. ) ;
#5800=UNCERTAINTY_MEASURE_WITH_UNIT (LENGTH_MEASURE( 1.000000000000000082E-05 ), #6568, 'distance_accuracy_value', 'NONE');
#5818=EDGE_CURVE ( 'NONE', #2858, #3174, #4598, .T. ) ;
#5855=DIRECTION ( 'NONE',  ( 1.000000000000000000, 0.000000000000000000, 0.000000000000000000 ) ) ;
#5864=EDGE_CURVE ( 'NONE', #2680, #2858, #7289, .T. ) ;
#5870=DIRECTION ( 'NONE',  ( 5.605193857299270773E-45, 0.000000000000000000, 1.000000000000000000 ) ) ;
#5893=CARTESIAN_POINT ( 'NONE',  ( 0.000000000000000000, 0.000000000000000000, -39.99999999999997868 ) ) ;
#5903=DIRECTION ( 'NONE',  ( 1.224646799147352714E-16, 1.000000000000000000, -6.864382715941954980E-61 ) ) ;
#5927=DIRECTION ( 'NONE',  ( 1.000000000000000000, 0.000000000000000000, 0.000000000000000000 ) ) ;
#6008=CARTESIAN_POINT ( 'NONE',  ( 0.000000000000000000, 0.000000000000000000, -9.999999999999994671 ) ) ;
#6098=DIRECTION ( 'NONE',  ( 1.000000000000000000, 0.000000000000000000, 0.000000000000000000 ) ) ;
#6108=ORIENTED_EDGE ( 'NONE', *, *, #2571, .F. ) ;
#6109=ORIENTED_EDGE ( 'NONE', *, *, #1081, .F. ) ;
#6151=DIRECTION ( 'NONE',  ( 5.605193857299270773E-45, 0.000000000000000000, 1.000000000000000000 ) ) ;
#6157=DIRECTION ( 'NONE',  ( 5.605193857299270773E-45, 0.000000000000000000, 1.000000000000000000 ) ) ;
#6162=CARTESIAN_POINT ( 'NONE',  ( 23.99999999999999289, 0.000000000000000000, 1.345246525751824388E-43 ) ) ;
#6230=ORIENTED_EDGE ( 'NONE', *, *, #3348, .F. ) ;
#6234=ORIENTED_EDGE ( 'NONE', *, *, #6723, .T. ) ;
#6237=CARTESIAN_POINT ( 'NONE',  ( 0.000000000000000000, 0.000000000000000000, 0.000000000000000000 ) ) ;
#6261=AXIS2_PLACEMENT_3D ( 'NONE', #823, #7325, #1904 ) ;
#6264=MANIFOLD_SOLID_BREP ( 'Fillet1', #3812 ) ;
#6270=DIRECTION ( 'NONE',  ( 5.605193857299270773E-45, 0.000000000000000000, 1.000000000000000000 ) ) ;
#6314=CARTESIAN_POINT ( 'NONE',  ( -17.99999999999999645, 2.204364238465234244E-15, -39.99999999999997868 ) ) ;
#6357=PRODUCT_DEFINITION_SHAPE ( 'NONE', 'NONE',  #1414 ) ;
#6359=DIRECTION ( 'NONE',  ( 5.605193857299270773E-45, 0.000000000000000000, 1.000000000000000000 ) ) ;
#6361=AXIS2_PLACEMENT_3D ( 'NONE', #5305, #2997, #3399 ) ;
#6362=ORIENTED_EDGE ( 'NONE', *, *, #3767, .F. ) ;
#6395=EDGE_CURVE ( 'NONE', #316, #1796, #2132, .T. ) ;
#6407=AXIS2_PLACEMENT_3D ( 'NONE', #2691, #6701, #4975 ) ;
#6415=UNCERTAINTY_MEASURE_WITH_UNIT (LENGTH_MEASURE( 1.000000000000000082E-05 ), #1708, 'distance_accuracy_value', 'NONE');
#6465=ORIENTED_EDGE ( 'NONE', *, *, #5818, .F. ) ;
#6492=EDGE_CURVE ( 'NONE', #2796, #316, #3871, .T. ) ;
#6494=DIRECTION ( 'NONE',  ( 1.000000000000000000, 0.000000000000000000, 0.000000000000000000 ) ) ;
#6512=EDGE_CURVE ( 'NONE', #1269, #1529, #7546, .T. ) ;
#6545=ADVANCED_FACE ( 'NONE', ( #555 ), #67, .T. ) ;
#6546=EDGE_CURVE ( 'NONE', #4861, #2624, #4368, .T. ) ;
#6560=DIRECTION ( 'NONE',  ( 5.605193857299270773E-45, 0.000000000000000000, 1.000000000000000000 ) ) ;
#6568=( LENGTH_UNIT ( ) NAMED_UNIT ( * ) SI_UNIT ( .MILLI., .METRE. ) );
#6577=VERTEX_POINT ( 'NONE', #4141 ) ;
#6605=CARTESIAN_POINT ( 'NONE',  ( 0.000000000000000000, 0.000000000000000000, -39.99999999999997868 ) ) ;
#6609=ADVANCED_FACE ( 'NONE', ( #4099 ), #1321, .T. ) ;
#6630=SHAPE_REPRESENTATION_RELATIONSHIP ( 'NONE' , 'NONE' ,  #97, #596 ) ;
#6632=DIRECTION ( 'NONE',  ( 5.605193857299270773E-45, 0.000000000000000000, 1.000000000000000000 ) ) ;
#6647=EDGE_LOOP ( 'NONE', ( #7313, #2273, #7187, #227 ) ) ;
#6656=AXIS2_PLACEMENT_3D ( 'NONE', #6605, #790, #222 ) ;
#6662=VECTOR ( 'NONE', #6763, 1000.000000000000000 ) ;
#6683=AXIS2_PLACEMENT_3D ( 'NONE', #115, #3538, #3035 ) ;
#6701=DIRECTION ( 'NONE',  ( 5.605193857299270773E-45, 0.000000000000000000, 1.000000000000000000 ) ) ;
#6723=EDGE_CURVE ( 'NONE', #1796, #2680, #3256, .T. ) ;
#6736=FACE_OUTER_BOUND ( 'NONE', #7196, .T. ) ;
#6750=CARTESIAN_POINT ( 'NONE',  ( -18.00000000000000000, 2.204364238465234639E-15, -9.999999999999994671 ) ) ;
#6763=DIRECTION ( 'NONE',  ( 5.605193857299270773E-45, 0.000000000000000000, 1.000000000000000000 ) ) ;
#6804=EDGE_LOOP ( 'NONE', ( #5477, #1526 ) ) ;
#6837=ORIENTED_EDGE ( 'NONE', *, *, #2571, .T. ) ;
#6843=CIRCLE ( 'NONE', #4148, 17.99999999999999645 ) ;
#6852=EDGE_CURVE ( 'NONE', #3174, #2858, #4860, .T. ) ;
#6858=CARTESIAN_POINT ( 'NONE',  ( -24.00000000000000000, 3.122849337825749433E-15, -9.999999999999994671 ) ) ;
#6865=DIRECTION ( 'NONE',  ( 5.605193857299270773E-45, 0.000000000000000000, 1.000000000000000000 ) ) ;
#6882=ORIENTED_EDGE ( 'NONE', *, *, #7295, .F. ) ;
#6887=ADVANCED_FACE ( 'NONE', ( #930 ), #3631, .T. ) ;
#6901=ORIENTED_EDGE ( 'NONE', *, *, #1961, .T. ) ;
#6983=DIRECTION ( 'NONE',  ( -1.000000000000000000, 1.224646799147353454E-16, 0.000000000000000000 ) ) ;
#6992=DIRECTION ( 'NONE',  ( 0.000000000000000000, -1.000000000000000000, 0.000000000000000000 ) ) ;
#6995=ORIENTED_EDGE ( 'NONE', *, *, #3767, .T. ) ;
#7006=ORIENTED_EDGE ( 'NONE', *, *, #6852, .F. ) ;
#7013=AXIS2_PLACEMENT_3D ( 'NONE', #3605, #6632, #6098 ) ;
#7030=DIRECTION ( 'NONE',  ( 5.605193857299270773E-45, 0.000000000000000000, 1.000000000000000000 ) ) ;
#7055=VECTOR ( 'NONE', #2648, 1000.000000000000000 ) ;
#7057=CARTESIAN_POINT ( 'NONE',  ( 0.000000000000000000, 0.000000000000000000, -6.999999999999992006 ) ) ;
#7122=ORIENTED_EDGE ( 'NONE', *, *, #1306, .T. ) ;
#7123=DIRECTION ( 'NONE',  ( 1.000000000000000000, 0.000000000000000000, 5.605193857299269528E-45 ) ) ;
#7160=DIRECTION ( 'NONE',  ( 5.605193857299270773E-45, 0.000000000000000000, 1.000000000000000000 ) ) ;
#7162=ORIENTED_EDGE ( 'NONE', *, *, #91, .F. ) ;
#7177=DIRECTION ( 'NONE',  ( 5.605193857299270773E-45, 0.000000000000000000, 1.000000000000000000 ) ) ;
#7178=CARTESIAN_POINT ( 'NONE',  ( 0.000000000000000000, 0.000000000000000000, -39.99999999999997868 ) ) ;
#7187=ORIENTED_EDGE ( 'NONE', *, *, #921, .T. ) ;
#7194=CARTESIAN_POINT ( 'NONE',  ( 26.99999999999999289, 0.000000000000000000, -6.999999999999992006 ) ) ;
#7196=EDGE_LOOP ( 'NONE', ( #6882, #7162, #5396, #7006 ) ) ;
#7234=ORIENTED_EDGE ( 'NONE', *, *, #6546, .F. ) ;
#7289=CIRCLE ( 'NONE', #53, 3.000000000000000000 ) ;
#7295=EDGE_CURVE ( 'NONE', #1796, #3174, #4002, .T. ) ;
#7313=ORIENTED_EDGE ( 'NONE', *, *, #6395, .F. ) ;
#7317=ADVANCED_FACE ( 'NONE', ( #4805 ), #4869, .T. ) ;
#7325=DIRECTION ( 'NONE',  ( -5.605193857299269528E-45, 0.000000000000000000, 1.000000000000000000 ) ) ;
#7334=DIRECTION ( 'NONE',  ( -5.605193857299270773E-45, -0.000000000000000000, -1.000000000000000000 ) ) ;
#7336=AXIS2_PLACEMENT_3D ( 'NONE', #5370, #3060, #57 ) ;
#7375=DIRECTION ( 'NONE',  ( 1.000000000000000000, 0.000000000000000000, 0.000000000000000000 ) ) ;
#7388=DIRECTION ( 'NONE',  ( 1.000000000000000000, 0.000000000000000000, -5.605193857299270773E-45 ) ) ;
#7413=APPLICATION_CONTEXT ( 'automotive_design' ) ;
#7414=AXIS2_PLACEMENT_3D ( 'NONE', #1150, #6359, #5927 ) ;
#7476=VERTEX_POINT ( 'NONE', #1551 ) ;
#7546=CIRCLE ( 'NONE', #4743, 13.99999999999999645 ) ;
#7555=CARTESIAN_POINT ( 'NONE',  ( -23.99999999999999289, 2.939152317953645922E-15, -6.999999999999992006 ) ) ;
#7646=COLOUR_RGB('Off White',0.89,0.88,0.83);
#7647=FILL_AREA_STYLE_COLOUR('',#7646);
#7648=FILL_AREA_STYLE('',(#7647));
#7649=SURFACE_STYLE_FILL_AREA(#7648);
#7650=SURFACE_SIDE_STYLE('',(#7649));
#7651=SURFACE_STYLE_USAGE(.BOTH.,#7650);
#7652=PRESENTATION_STYLE_ASSIGNMENT((#7651));
ENDSEC;
END-ISO-10303-21;
